ISO-10303-21;
HEADER;
/* Generated by software containing ST-Developer
 * from STEP Tools, Inc. (www.steptools.com) 
 */

FILE_DESCRIPTION(
/* description */ ('Belt-driven linear axis on 2020 extrusion'),
/* implementation_level */ '2;1');

FILE_NAME(
/* name */ 'Input M3 set screw (2).step',
/* time_stamp */ '2026-10-28T03:26:09-07:00',
/* author */ (''),
/* organization */ (''),
/* preprocessor_version */ 'ST-DEVELOPER v20.2',
/* originating_system */ 'Autodesk Translation Framework v15.17.0.0',
/* authorisation */ '');

FILE_SCHEMA (('AUTOMOTIVE_DESIGN { 1 0 10303 214 3 1 1 }'));
ENDSEC;

DATA;
#10=MECHANICAL_DESIGN_GEOMETRIC_PRESENTATION_REPRESENTATION('',(#652),#20096);
#550=SHAPE_REPRESENTATION_RELATIONSHIP('SRR','None',#20349,#596);
#596=ADVANCED_BREP_SHAPE_REPRESENTATION('',(#707),#20080);
#652=STYLED_ITEM('',(#20657),#707);
#707=MANIFOLD_SOLID_BREP('Body1',#10966);
#1138=PLANE('',#12303);
#1139=PLANE('',#12304);
#1670=FACE_OUTER_BOUND('',#2423,.T.);
#1671=FACE_OUTER_BOUND('',#2424,.T.);
#1672=FACE_OUTER_BOUND('',#2425,.T.);
#2423=EDGE_LOOP('',(#9109,#9110,#9111,#9112));
#2424=EDGE_LOOP('',(#9113));
#2425=EDGE_LOOP('',(#9114));
#3228=LINE('',#18592,#4085);
#4085=VECTOR('',#14972,0.149999999999999);
#4724=CIRCLE('',#12301,0.149999999999999);
#4725=CIRCLE('',#12302,0.149999999999999);
#5519=VERTEX_POINT('',#18589);
#5520=VERTEX_POINT('',#18591);
#6769=EDGE_CURVE('',#5519,#5519,#4724,.T.);
#6770=EDGE_CURVE('',#5519,#5520,#3228,.T.);
#6771=EDGE_CURVE('',#5520,#5520,#4725,.T.);
#9109=ORIENTED_EDGE('',*,*,#6769,.F.);
#9110=ORIENTED_EDGE('',*,*,#6770,.T.);
#9111=ORIENTED_EDGE('',*,*,#6771,.T.);
#9112=ORIENTED_EDGE('',*,*,#6770,.F.);
#9113=ORIENTED_EDGE('',*,*,#6769,.T.);
#9114=ORIENTED_EDGE('',*,*,#6771,.F.);
#10223=CYLINDRICAL_SURFACE('',#12300,0.149999999999999);
#10721=ADVANCED_FACE('',(#1670),#10223,.T.);
#10722=ADVANCED_FACE('',(#1671),#1138,.T.);
#10723=ADVANCED_FACE('',(#1672),#1139,.F.);
#10966=CLOSED_SHELL('',(#10721,#10722,#10723));
#12299=AXIS2_PLACEMENT_3D('',#18587,#14966,#14967);
#12300=AXIS2_PLACEMENT_3D('',#18588,#14968,#14969);
#12301=AXIS2_PLACEMENT_3D('',#18590,#14970,#14971);
#12302=AXIS2_PLACEMENT_3D('',#18593,#14973,#14974);
#12303=AXIS2_PLACEMENT_3D('',#18594,#14975,#14976);
#12304=AXIS2_PLACEMENT_3D('',#18595,#14977,#14978);
#14966=DIRECTION('axis',(0.,0.,1.));
#14967=DIRECTION('refdir',(1.,0.,0.));
#14968=DIRECTION('center_axis',(0.,0.,1.));
#14969=DIRECTION('ref_axis',(1.,0.,0.));
#14970=DIRECTION('center_axis',(0.,0.,1.));
#14971=DIRECTION('ref_axis',(1.,0.,0.));
#14972=DIRECTION('',(0.,0.,-1.));
#14973=DIRECTION('center_axis',(0.,0.,1.));
#14974=DIRECTION('ref_axis',(1.,0.,0.));
#14975=DIRECTION('center_axis',(0.,0.,1.));
#14976=DIRECTION('ref_axis',(1.,0.,0.));
#14977=DIRECTION('center_axis',(0.,0.,1.));
#14978=DIRECTION('ref_axis',(1.,0.,0.));
#18587=CARTESIAN_POINT('',(0.,0.,0.));
#18588=CARTESIAN_POINT('Origin',(32.,-3.95,6.35));
#18589=CARTESIAN_POINT('',(31.85,-3.95,6.6));
#18590=CARTESIAN_POINT('Origin',(32.,-3.95,6.6));
#18591=CARTESIAN_POINT('',(31.85,-3.95,6.35));
#18592=CARTESIAN_POINT('',(31.85,-3.95,6.35));
#18593=CARTESIAN_POINT('Origin',(32.,-3.95,6.35));
#18594=CARTESIAN_POINT('Origin',(32.,-3.95,6.6));
#18595=CARTESIAN_POINT('Origin',(32.,-3.95,6.35));
#20026=UNCERTAINTY_MEASURE_WITH_UNIT(LENGTH_MEASURE(0.001),#20097,
'DISTANCE_ACCURACY_VALUE',
'Maximum model space distance between geometric entities at asserted c
onnectivities');
#20042=UNCERTAINTY_MEASURE_WITH_UNIT(LENGTH_MEASURE(0.001),#20097,
'DISTANCE_ACCURACY_VALUE',
'Maximum model space distance between geometric entities at asserted c
onnectivities');
#20080=(
GEOMETRIC_REPRESENTATION_CONTEXT(3)
GLOBAL_UNCERTAINTY_ASSIGNED_CONTEXT((#20026))
GLOBAL_UNIT_ASSIGNED_CONTEXT((#20097,#20099,#20100))
REPRESENTATION_CONTEXT('','3D')
);
#20096=(
GEOMETRIC_REPRESENTATION_CONTEXT(3)
GLOBAL_UNCERTAINTY_ASSIGNED_CONTEXT((#20042))
GLOBAL_UNIT_ASSIGNED_CONTEXT((#20097,#20099,#20100))
REPRESENTATION_CONTEXT('','3D')
);
#20097=(
LENGTH_UNIT()
NAMED_UNIT(*)
SI_UNIT(.CENTI.,.METRE.)
);
#20099=(
NAMED_UNIT(*)
PLANE_ANGLE_UNIT()
SI_UNIT($,.RADIAN.)
);
#20100=(
NAMED_UNIT(*)
SI_UNIT($,.STERADIAN.)
SOLID_ANGLE_UNIT()
);
#20138=SHAPE_DEFINITION_REPRESENTATION(#20196,#20349);
#20196=PRODUCT_DEFINITION_SHAPE('',$,#20403);
#20349=SHAPE_REPRESENTATION('',(#12299),#20080);
#20365=PRODUCT_DEFINITION_CONTEXT('part definition',#20526,'design');
#20403=PRODUCT_DEFINITION('Input M3 set screw (2)',
'Input M3 set screw (2)',#20456,#20365);
#20456=PRODUCT_DEFINITION_FORMATION('',$,#20565);
#20526=APPLICATION_CONTEXT(
'Core Data for Automotive Mechanical Design Process');
#20527=PRODUCT_CONTEXT('part definition',#20526,'mechanical');
#20565=PRODUCT('Input M3 set screw (2)','Input M3 set screw (2)',
'Input M3 set screw (2)',(#20527));
#20651=COLOUR_RGB('Black',0.12,0.14,0.17);
#20652=FILL_AREA_STYLE_COLOUR('',#20651);
#20653=FILL_AREA_STYLE('',(#20652));
#20654=SURFACE_STYLE_FILL_AREA(#20653);
#20655=SURFACE_SIDE_STYLE('',(#20654));
#20656=SURFACE_STYLE_USAGE(.BOTH.,#20655);
#20657=PRESENTATION_STYLE_ASSIGNMENT((#20656));
ENDSEC;
END-ISO-10303-21;
